ISO-10303-21;
HEADER;
FILE_DESCRIPTION (('STEP AP203'),
    '1' );
FILE_NAME ('bench vise6_3-.step',
    '2026-10-07T23:37:23',
    ( '' ),
    ( '' ),
    'SwSTEP 2.0',
    'SolidWorks 2024',
    '' );
FILE_SCHEMA (( 'AUTOMOTIVE_DESIGN' ));
ENDSEC;

DATA;
#224=EDGE_CURVE ( 'NONE', #539, #2109, #923, .T. ) ;
#236=CARTESIAN_POINT ( 'NONE',  ( 2.537500000000000533, 2.500000000000000444, 0.000000000000000000 ) ) ;
#371=( NAMED_UNIT ( * ) SI_UNIT ( $, .STERADIAN. ) SOLID_ANGLE_UNIT ( ) );
#377=CARTESIAN_POINT ( 'NONE',  ( 2.537500000000000533, 2.500000000000000444, -0.4312500000000004663 ) ) ;
#397=PLANE ( 'NONE',  #2958 ) ;
#428=FACE_OUTER_BOUND ( 'NONE', #3311, .T. ) ;
#539=VERTEX_POINT ( 'NONE', #4472 ) ;
#549=ADVANCED_BREP_SHAPE_REPRESENTATION ( '', ( #7369, #7272 ), #3475 ) ;
#551=CARTESIAN_POINT ( 'NONE',  ( 2.537500000000000533, 4.049999999999999822, 0.4312500000000004663 ) ) ;
#737=EDGE_LOOP ( 'NONE', ( #4760, #2818, #4208, #7975 ) ) ;
#861=ORIENTED_EDGE ( 'NONE', *, *, #4247, .T. ) ;
#907=DIRECTION ( 'NONE',  ( 0.000000000000000000, 1.000000000000000000, 0.000000000000000000 ) ) ;
#923=LINE ( 'NONE', #3422, #5293 ) ;
#1072=( LENGTH_UNIT ( ) NAMED_UNIT ( * ) SI_UNIT ( $, .METRE. ) );
#1122=DIRECTION ( 'NONE',  ( 0.000000000000000000, 1.000000000000000000, 0.000000000000000000 ) ) ;
#1175=CARTESIAN_POINT ( 'NONE',  ( 2.537500000000000533, 4.049999999999999822, 0.000000000000000000 ) ) ;
#1185=DIRECTION ( 'NONE',  ( 0.000000000000000000, 0.000000000000000000, 1.000000000000000000 ) ) ;
#1217=AXIS2_PLACEMENT_3D ( 'NONE', #7608, #6265, #1185 ) ;
#1406=CIRCLE ( 'NONE', #6769, 0.4312500000000004663 ) ;
#1451=UNCERTAINTY_MEASURE_WITH_UNIT (LENGTH_MEASURE( 1.000000000000000082E-05 ), #3612, 'distance_accuracy_value', 'NONE');
#1817=DIRECTION ( 'NONE',  ( 0.000000000000000000, 1.000000000000000000, 0.000000000000000000 ) ) ;
#1857=VERTEX_POINT ( 'NONE', #6224 ) ;
#2006=CIRCLE ( 'NONE', #6604, 0.4312500000000004663 ) ;
#2014=ORIENTED_EDGE ( 'NONE', *, *, #3180, .F. ) ;
#2018=ADVANCED_FACE ( 'N', ( #3999 ), #397, .T. ) ;
#2109=VERTEX_POINT ( 'NONE', #551 ) ;
#2180=LINE ( 'NONE', #4046, #7816 ) ;
#2205=EDGE_CURVE ( 'NONE', #2109, #1857, #1406, .T. ) ;
#2350=DIRECTION ( 'NONE',  ( -0.000000000000000000, -1.000000000000000000, -0.000000000000000000 ) ) ;
#2436=FACE_OUTER_BOUND ( 'NONE', #5782, .T. ) ;
#2542=EDGE_CURVE ( 'NONE', #3034, #539, #7717, .T. ) ;
#2818=ORIENTED_EDGE ( 'NONE', *, *, #2542, .T. ) ;
#2921=DIRECTION ( 'NONE',  ( 0.000000000000000000, 1.000000000000000000, 0.000000000000000000 ) ) ;
#2958=AXIS2_PLACEMENT_3D ( 'NONE', #4114, #6641, #7863 ) ;
#3034=VERTEX_POINT ( 'NONE', #377 ) ;
#3180=EDGE_CURVE ( 'NONE', #1857, #2109, #2006, .T. ) ;
#3265=DIRECTION ( 'NONE',  ( 0.000000000000000000, 1.000000000000000000, 0.000000000000000000 ) ) ;
#3311=EDGE_LOOP ( 'NONE', ( #861, #7235, #3385, #3777 ) ) ;
#3385=ORIENTED_EDGE ( 'NONE', *, *, #3180, .T. ) ;
#3422=CARTESIAN_POINT ( 'NONE',  ( 2.537500000000000533, 2.500000000000000444, 0.4312500000000004663 ) ) ;
#3475=( GEOMETRIC_REPRESENTATION_CONTEXT ( 3 ) GLOBAL_UNCERTAINTY_ASSIGNED_CONTEXT ( ( #1451 ) ) GLOBAL_UNIT_ASSIGNED_CONTEXT ( ( #3612, #8088, #371 ) ) REPRESENTATION_CONTEXT ( 'NONE', 'WORKASPACE' ) );
#3482=ORIENTED_EDGE ( 'NONE', *, *, #2542, .F. ) ;
#3563=SHAPE_REPRESENTATION_RELATIONSHIP ( 'NONE' , 'NONE' ,  #6969, #549 ) ;
#3612=( CONVERSION_BASED_UNIT ( 'INCH', #4300 ) LENGTH_UNIT ( ) NAMED_UNIT ( #6273 ) );
#3659=CARTESIAN_POINT ( 'NONE',  ( 2.537500000000000533, 2.500000000000000444, 0.000000000000000000 ) ) ;
#3685=CYLINDRICAL_SURFACE ( 'NONE', #1217, 0.4312500000000004663 ) ;
#3719=CIRCLE ( 'NONE', #5414, 0.4312500000000004663 ) ;
#3736=CARTESIAN_POINT ( 'NONE',  ( 0.000000000000000000, 0.000000000000000000, 0.000000000000000000 ) ) ;
#3777=ORIENTED_EDGE ( 'NONE', *, *, #224, .F. ) ;
#3896=PRODUCT ( 'bench vise6_3-', 'bench vise6_3-', '', ( #4972 ) ) ;
#3999=FACE_OUTER_BOUND ( 'NONE', #6539, .T. ) ;
#4046=CARTESIAN_POINT ( 'NONE',  ( 2.537500000000000533, 2.500000000000000444, -0.4312500000000004663 ) ) ;
#4105=DIRECTION ( 'NONE',  ( 0.000000000000000000, 0.000000000000000000, 1.000000000000000000 ) ) ;
#4114=CARTESIAN_POINT ( 'NONE',  ( 2.968750000000001332, 2.500000000000000444, 0.000000000000000000 ) ) ;
#4208=ORIENTED_EDGE ( 'NONE', *, *, #224, .T. ) ;
#4247=EDGE_CURVE ( 'NONE', #539, #3034, #3719, .T. ) ;
#4300=LENGTH_MEASURE_WITH_UNIT ( LENGTH_MEASURE( 0.02539999999999999897 ), #1072 );
#4309=DIRECTION ( 'NONE',  ( 0.000000000000000000, -0.000000000000000000, 1.000000000000000000 ) ) ;
#4472=CARTESIAN_POINT ( 'NONE',  ( 2.537500000000000533, 2.500000000000000444, 0.4312500000000004663 ) ) ;
#4583=EDGE_CURVE ( 'NONE', #3034, #1857, #2180, .T. ) ;
#4664=AXIS2_PLACEMENT_3D ( 'NONE', #236, #3265, #7044 ) ;
#4760=ORIENTED_EDGE ( 'NONE', *, *, #4583, .F. ) ;
#4938=DIRECTION ( 'NONE',  ( -0.000000000000000000, -1.000000000000000000, -0.000000000000000000 ) ) ;
#4972=MECHANICAL_CONTEXT ( 'NONE', #7363, 'mechanical' ) ;
#5293=VECTOR ( 'NONE', #6510, 39.37007874015748143 ) ;
#5310=PRODUCT_DEFINITION ( 'UNKNOWN', '', #5941, #6037 ) ;
#5375=CARTESIAN_POINT ( 'NONE',  ( 2.537500000000000533, 2.500000000000000444, 0.000000000000000000 ) ) ;
#5414=AXIS2_PLACEMENT_3D ( 'NONE', #3659, #1122, #6236 ) ;
#5538=ADVANCED_FACE ( 'NONE', ( #428 ), #7378, .T. ) ;
#5618=DIRECTION ( 'NONE',  ( 1.000000000000000000, 0.000000000000000000, 0.000000000000000000 ) ) ;
#5690=CLOSED_SHELL ( 'NONE', ( #5538, #7489, #8095, #2018 ) ) ;
#5705=ORIENTED_EDGE ( 'NONE', *, *, #2205, .F. ) ;
#5782=EDGE_LOOP ( 'NONE', ( #5705, #2014 ) ) ;
#5941=PRODUCT_DEFINITION_FORMATION_WITH_SPECIFIED_SOURCE ( 'ANY', '', #3896, .NOT_KNOWN. ) ;
#5975=APPLICATION_CONTEXT ( 'configuration controlled 3d designs of mechanical parts and assemblies' ) ;
#6037=DESIGN_CONTEXT ( 'detailed design', #5975, 'design' ) ;
#6074=CARTESIAN_POINT ( 'NONE',  ( 2.537500000000000533, 4.049999999999999822, 0.000000000000000000 ) ) ;
#6132=SHAPE_DEFINITION_REPRESENTATION ( #8039, #6969 ) ;
#6194=CARTESIAN_POINT ( 'NONE',  ( 2.537500000000000533, 4.049999999999999822, 0.000000000000000000 ) ) ;
#6224=CARTESIAN_POINT ( 'NONE',  ( 2.537500000000000533, 4.049999999999999822, -0.4312500000000004663 ) ) ;
#6236=DIRECTION ( 'NONE',  ( 0.000000000000000000, 0.000000000000000000, 1.000000000000000000 ) ) ;
#6237=DIRECTION ( 'NONE',  ( 0.000000000000000000, 0.000000000000000000, 1.000000000000000000 ) ) ;
#6265=DIRECTION ( 'NONE',  ( 0.000000000000000000, 1.000000000000000000, 0.000000000000000000 ) ) ;
#6273=DIMENSIONAL_EXPONENTS ( 1.000000000000000000, 0.000000000000000000, 0.000000000000000000, 0.000000000000000000, 0.000000000000000000, 0.000000000000000000, 0.000000000000000000 ) ;
#6510=DIRECTION ( 'NONE',  ( 0.000000000000000000, 1.000000000000000000, 0.000000000000000000 ) ) ;
#6539=EDGE_LOOP ( 'NONE', ( #6869, #3482 ) ) ;
#6604=AXIS2_PLACEMENT_3D ( 'NONE', #6074, #2350, #7366 ) ;
#6641=DIRECTION ( 'NONE',  ( 0.000000000000000000, -1.000000000000000000, 0.000000000000000000 ) ) ;
#6769=AXIS2_PLACEMENT_3D ( 'NONE', #1175, #4938, #7481 ) ;
#6801=FACE_OUTER_BOUND ( 'NONE', #737, .T. ) ;
#6869=ORIENTED_EDGE ( 'NONE', *, *, #4247, .F. ) ;
#6969=SHAPE_REPRESENTATION ( 'bench vise6_3-', ( #7272 ), #3475 ) ;
#7044=DIRECTION ( 'NONE',  ( 0.000000000000000000, 0.000000000000000000, 1.000000000000000000 ) ) ;
#7235=ORIENTED_EDGE ( 'NONE', *, *, #4583, .T. ) ;
#7272=AXIS2_PLACEMENT_3D ( 'NONE', #3736, #6237, #5618 ) ;
#7329=PLANE ( 'NONE',  #7677 ) ;
#7363=APPLICATION_CONTEXT ( 'configuration controlled 3d designs of mechanical parts and assemblies' ) ;
#7366=DIRECTION ( 'NONE',  ( 0.000000000000000000, 0.000000000000000000, 1.000000000000000000 ) ) ;
#7369=MANIFOLD_SOLID_BREP ( 'Imported1', #5690 ) ;
#7378=CYLINDRICAL_SURFACE ( 'NONE', #7671, 0.4312500000000004663 ) ;
#7481=DIRECTION ( 'NONE',  ( 0.000000000000000000, 0.000000000000000000, 1.000000000000000000 ) ) ;
#7489=ADVANCED_FACE ( 'NONE', ( #6801 ), #3685, .T. ) ;
#7608=CARTESIAN_POINT ( 'NONE',  ( 2.537500000000000533, 2.500000000000000444, 0.000000000000000000 ) ) ;
#7671=AXIS2_PLACEMENT_3D ( 'NONE', #5375, #2921, #4105 ) ;
#7677=AXIS2_PLACEMENT_3D ( 'NONE', #6194, #1817, #4309 ) ;
#7717=CIRCLE ( 'NONE', #4664, 0.4312500000000004663 ) ;
#7816=VECTOR ( 'NONE', #907, 39.37007874015748143 ) ;
#7863=DIRECTION ( 'NONE',  ( 0.000000000000000000, -0.000000000000000000, -1.000000000000000000 ) ) ;
#7975=ORIENTED_EDGE ( 'NONE', *, *, #2205, .T. ) ;
#8039=PRODUCT_DEFINITION_SHAPE ( 'NONE', 'NONE',  #5310 ) ;
#8088=( NAMED_UNIT ( * ) PLANE_ANGLE_UNIT ( ) SI_UNIT ( $, .RADIAN. ) );
#8095=ADVANCED_FACE ( 'NONE', ( #2436 ), #7329, .T. ) ;
#8213=COLOUR_RGB('Sky Blue', 0.40784314, 0.44705882, 0.49803922);
#8214=FILL_AREA_STYLE_COLOUR('',#8213);
#8215=FILL_AREA_STYLE('',(#8214));
#8216=SURFACE_STYLE_FILL_AREA(#8215);
#8217=SURFACE_SIDE_STYLE('',(#8216));
#8218=SURFACE_STYLE_USAGE(.BOTH.,#8217);
#8219=PRESENTATION_STYLE_ASSIGNMENT((#8218));
#8241=STYLED_ITEM('',(#8219),#7369);
#8242=MECHANICAL_DESIGN_GEOMETRIC_PRESENTATION_REPRESENTATION('',(#8241),#3475);
ENDSEC;
END-ISO-10303-21;
